ISO-10303-21;
HEADER;
/* Generated by software containing ST-Developer
 * from STEP Tools, Inc. (www.steptools.com) 
 */

FILE_DESCRIPTION(
/* description */ ('Belt-driven linear axis on 2020 extrusion'),
/* implementation_level */ '2;1');

FILE_NAME(
/* name */ 'M4x10 Cap Screw.step',
/* time_stamp */ '2026-10-28T03:26:09-07:00',
/* author */ (''),
/* organization */ (''),
/* preprocessor_version */ 'ST-DEVELOPER v20.2',
/* originating_system */ 'Autodesk Translation Framework v15.17.0.0',
/* authorisation */ '');

FILE_SCHEMA (('AUTOMOTIVE_DESIGN { 1 0 10303 214 3 1 1 }'));
ENDSEC;

DATA;
#10=MECHANICAL_DESIGN_GEOMETRIC_PRESENTATION_REPRESENTATION('',(#664),#20096);
#13=ORIENTED_CLOSED_SHELL('',*,#10979,.F.);
#17=BREP_WITH_VOIDS('Body1',#10980,(#13));
#509=CONICAL_SURFACE('',#12651,0.325,0.785398163397448);
#510=CONICAL_SURFACE('',#12655,0.335,0.785398163397448);
#511=CONICAL_SURFACE('',#12659,0.21,0.463647609000806);
#562=SHAPE_REPRESENTATION_RELATIONSHIP('SRR','None',#20363,#608);
#608=ADVANCED_BREP_SHAPE_REPRESENTATION('',(#17),#20094);
#664=STYLED_ITEM('',(#20657),#17);
#887=FACE_BOUND('',#2644,.T.);
#1228=PLANE('',#12639);
#1229=PLANE('',#12640);
#1230=PLANE('',#12641);
#1231=PLANE('',#12642);
#1232=PLANE('',#12643);
#1233=PLANE('',#12644);
#1234=PLANE('',#12645);
#1235=PLANE('',#12646);
#1236=PLANE('',#12647);
#1237=PLANE('',#12649);
#1238=PLANE('',#12657);
#1839=FACE_OUTER_BOUND('',#2630,.T.);
#1840=FACE_OUTER_BOUND('',#2631,.T.);
#1841=FACE_OUTER_BOUND('',#2632,.T.);
#1842=FACE_OUTER_BOUND('',#2633,.T.);
#1843=FACE_OUTER_BOUND('',#2634,.T.);
#1844=FACE_OUTER_BOUND('',#2635,.T.);
#1845=FACE_OUTER_BOUND('',#2636,.T.);
#1846=FACE_OUTER_BOUND('',#2637,.T.);
#1847=FACE_OUTER_BOUND('',#2638,.T.);
#1848=FACE_OUTER_BOUND('',#2639,.T.);
#1849=FACE_OUTER_BOUND('',#2640,.T.);
#1850=FACE_OUTER_BOUND('',#2641,.T.);
#1851=FACE_OUTER_BOUND('',#2642,.T.);
#1852=FACE_OUTER_BOUND('',#2643,.T.);
#1853=FACE_OUTER_BOUND('',#2645,.T.);
#1854=FACE_OUTER_BOUND('',#2646,.T.);
#2630=EDGE_LOOP('',(#9953,#9954,#9955,#9956));
#2631=EDGE_LOOP('',(#9957,#9958,#9959,#9960));
#2632=EDGE_LOOP('',(#9961,#9962,#9963,#9964));
#2633=EDGE_LOOP('',(#9965,#9966,#9967,#9968));
#2634=EDGE_LOOP('',(#9969,#9970,#9971,#9972));
#2635=EDGE_LOOP('',(#9973,#9974,#9975,#9976));
#2636=EDGE_LOOP('',(#9977,#9978,#9979,#9980,#9981,#9982));
#2637=EDGE_LOOP('',(#9983,#9984,#9985,#9986,#9987,#9988));
#2638=EDGE_LOOP('',(#9989));
#2639=EDGE_LOOP('',(#9990));
#2640=EDGE_LOOP('',(#9991,#9992,#9993,#9994));
#2641=EDGE_LOOP('',(#9995,#9996,#9997,#9998));
#2642=EDGE_LOOP('',(#9999,#10000,#10001,#10002));
#2643=EDGE_LOOP('',(#10003));
#2644=EDGE_LOOP('',(#10004));
#2645=EDGE_LOOP('',(#10005,#10006,#10007,#10008));
#2646=EDGE_LOOP('',(#10009,#10010,#10011,#10012));
#3475=LINE('',#19760,#4332);
#3476=LINE('',#19762,#4333);
#3477=LINE('',#19764,#4334);
#3478=LINE('',#19765,#4335);
#3479=LINE('',#19768,#4336);
#3480=LINE('',#19770,#4337);
#3481=LINE('',#19771,#4338);
#3482=LINE('',#19774,#4339);
#3483=LINE('',#19776,#4340);
#3484=LINE('',#19777,#4341);
#3485=LINE('',#19780,#4342);
#3486=LINE('',#19782,#4343);
#3487=LINE('',#19783,#4344);
#3488=LINE('',#19786,#4345);
#3489=LINE('',#19788,#4346);
#3490=LINE('',#19789,#4347);
#3491=LINE('',#19791,#4348);
#3492=LINE('',#19792,#4349);
#3493=LINE('',#19804,#4350);
#3494=LINE('',#19808,#4351);
#3495=LINE('',#19812,#4352);
#3496=LINE('',#19819,#4353);
#3497=LINE('',#19821,#4354);
#4332=VECTOR('',#15895,1.);
#4333=VECTOR('',#15896,1.);
#4334=VECTOR('',#15897,1.);
#4335=VECTOR('',#15898,1.);
#4336=VECTOR('',#15901,1.);
#4337=VECTOR('',#15902,1.);
#4338=VECTOR('',#15903,1.);
#4339=VECTOR('',#15906,1.);
#4340=VECTOR('',#15907,1.);
#4341=VECTOR('',#15908,1.);
#4342=VECTOR('',#15911,1.);
#4343=VECTOR('',#15912,1.);
#4344=VECTOR('',#15913,1.);
#4345=VECTOR('',#15916,1.);
#4346=VECTOR('',#15917,1.);
#4347=VECTOR('',#15918,1.);
#4348=VECTOR('',#15921,1.);
#4349=VECTOR('',#15922,1.);
#4350=VECTOR('',#15939,0.325);
#4351=VECTOR('',#15944,0.35);
#4352=VECTOR('',#15949,0.335);
#4353=VECTOR('',#15958,0.21);
#4354=VECTOR('',#15961,0.2);
#4877=CIRCLE('',#12648,0.1954);
#4878=CIRCLE('',#12650,0.3);
#4879=CIRCLE('',#12652,0.35);
#4880=CIRCLE('',#12654,0.35);
#4881=CIRCLE('',#12656,0.32);
#4882=CIRCLE('',#12658,0.22);
#4883=CIRCLE('',#12660,0.1954);
#5802=VERTEX_POINT('',#19758);
#5803=VERTEX_POINT('',#19759);
#5804=VERTEX_POINT('',#19761);
#5805=VERTEX_POINT('',#19763);
#5806=VERTEX_POINT('',#19767);
#5807=VERTEX_POINT('',#19769);
#5808=VERTEX_POINT('',#19773);
#5809=VERTEX_POINT('',#19775);
#5810=VERTEX_POINT('',#19779);
#5811=VERTEX_POINT('',#19781);
#5812=VERTEX_POINT('',#19785);
#5813=VERTEX_POINT('',#19787);
#5814=VERTEX_POINT('',#19796);
#5815=VERTEX_POINT('',#19799);
#5816=VERTEX_POINT('',#19802);
#5817=VERTEX_POINT('',#19806);
#5818=VERTEX_POINT('',#19810);
#5819=VERTEX_POINT('',#19814);
#5820=VERTEX_POINT('',#19817);
#7191=EDGE_CURVE('',#5802,#5803,#3475,.T.);
#7192=EDGE_CURVE('',#5803,#5804,#3476,.T.);
#7193=EDGE_CURVE('',#5804,#5805,#3477,.T.);
#7194=EDGE_CURVE('',#5802,#5805,#3478,.T.);
#7195=EDGE_CURVE('',#5803,#5806,#3479,.T.);
#7196=EDGE_CURVE('',#5806,#5807,#3480,.T.);
#7197=EDGE_CURVE('',#5807,#5804,#3481,.T.);
#7198=EDGE_CURVE('',#5806,#5808,#3482,.T.);
#7199=EDGE_CURVE('',#5808,#5809,#3483,.T.);
#7200=EDGE_CURVE('',#5809,#5807,#3484,.T.);
#7201=EDGE_CURVE('',#5808,#5810,#3485,.T.);
#7202=EDGE_CURVE('',#5810,#5811,#3486,.T.);
#7203=EDGE_CURVE('',#5811,#5809,#3487,.T.);
#7204=EDGE_CURVE('',#5810,#5812,#3488,.T.);
#7205=EDGE_CURVE('',#5812,#5813,#3489,.T.);
#7206=EDGE_CURVE('',#5813,#5811,#3490,.T.);
#7207=EDGE_CURVE('',#5812,#5802,#3491,.T.);
#7208=EDGE_CURVE('',#5805,#5813,#3492,.T.);
#7209=EDGE_CURVE('',#5814,#5814,#4877,.T.);
#7210=EDGE_CURVE('',#5815,#5815,#4878,.T.);
#7211=EDGE_CURVE('',#5816,#5816,#4879,.T.);
#7212=EDGE_CURVE('',#5816,#5815,#3493,.T.);
#7213=EDGE_CURVE('',#5817,#5817,#4880,.T.);
#7214=EDGE_CURVE('',#5817,#5816,#3494,.T.);
#7215=EDGE_CURVE('',#5818,#5818,#4881,.T.);
#7216=EDGE_CURVE('',#5818,#5817,#3495,.T.);
#7217=EDGE_CURVE('',#5819,#5819,#4882,.T.);
#7218=EDGE_CURVE('',#5820,#5820,#4883,.F.);
#7219=EDGE_CURVE('',#5820,#5819,#3496,.T.);
#7220=EDGE_CURVE('',#5814,#5820,#3497,.T.);
#9953=ORIENTED_EDGE('',*,*,#7191,.T.);
#9954=ORIENTED_EDGE('',*,*,#7192,.T.);
#9955=ORIENTED_EDGE('',*,*,#7193,.T.);
#9956=ORIENTED_EDGE('',*,*,#7194,.F.);
#9957=ORIENTED_EDGE('',*,*,#7195,.T.);
#9958=ORIENTED_EDGE('',*,*,#7196,.T.);
#9959=ORIENTED_EDGE('',*,*,#7197,.T.);
#9960=ORIENTED_EDGE('',*,*,#7192,.F.);
#9961=ORIENTED_EDGE('',*,*,#7198,.T.);
#9962=ORIENTED_EDGE('',*,*,#7199,.T.);
#9963=ORIENTED_EDGE('',*,*,#7200,.T.);
#9964=ORIENTED_EDGE('',*,*,#7196,.F.);
#9965=ORIENTED_EDGE('',*,*,#7201,.T.);
#9966=ORIENTED_EDGE('',*,*,#7202,.T.);
#9967=ORIENTED_EDGE('',*,*,#7203,.T.);
#9968=ORIENTED_EDGE('',*,*,#7199,.F.);
#9969=ORIENTED_EDGE('',*,*,#7204,.T.);
#9970=ORIENTED_EDGE('',*,*,#7205,.T.);
#9971=ORIENTED_EDGE('',*,*,#7206,.T.);
#9972=ORIENTED_EDGE('',*,*,#7202,.F.);
#9973=ORIENTED_EDGE('',*,*,#7207,.T.);
#9974=ORIENTED_EDGE('',*,*,#7194,.T.);
#9975=ORIENTED_EDGE('',*,*,#7208,.T.);
#9976=ORIENTED_EDGE('',*,*,#7205,.F.);
#9977=ORIENTED_EDGE('',*,*,#7207,.F.);
#9978=ORIENTED_EDGE('',*,*,#7204,.F.);
#9979=ORIENTED_EDGE('',*,*,#7201,.F.);
#9980=ORIENTED_EDGE('',*,*,#7198,.F.);
#9981=ORIENTED_EDGE('',*,*,#7195,.F.);
#9982=ORIENTED_EDGE('',*,*,#7191,.F.);
#9983=ORIENTED_EDGE('',*,*,#7208,.F.);
#9984=ORIENTED_EDGE('',*,*,#7193,.F.);
#9985=ORIENTED_EDGE('',*,*,#7197,.F.);
#9986=ORIENTED_EDGE('',*,*,#7200,.F.);
#9987=ORIENTED_EDGE('',*,*,#7203,.F.);
#9988=ORIENTED_EDGE('',*,*,#7206,.F.);
#9989=ORIENTED_EDGE('',*,*,#7209,.F.);
#9990=ORIENTED_EDGE('',*,*,#7210,.F.);
#9991=ORIENTED_EDGE('',*,*,#7211,.F.);
#9992=ORIENTED_EDGE('',*,*,#7212,.T.);
#9993=ORIENTED_EDGE('',*,*,#7210,.T.);
#9994=ORIENTED_EDGE('',*,*,#7212,.F.);
#9995=ORIENTED_EDGE('',*,*,#7213,.F.);
#9996=ORIENTED_EDGE('',*,*,#7214,.T.);
#9997=ORIENTED_EDGE('',*,*,#7211,.T.);
#9998=ORIENTED_EDGE('',*,*,#7214,.F.);
#9999=ORIENTED_EDGE('',*,*,#7215,.F.);
#10000=ORIENTED_EDGE('',*,*,#7216,.T.);
#10001=ORIENTED_EDGE('',*,*,#7213,.T.);
#10002=ORIENTED_EDGE('',*,*,#7216,.F.);
#10003=ORIENTED_EDGE('',*,*,#7215,.T.);
#10004=ORIENTED_EDGE('',*,*,#7217,.F.);
#10005=ORIENTED_EDGE('',*,*,#7218,.F.);
#10006=ORIENTED_EDGE('',*,*,#7219,.T.);
#10007=ORIENTED_EDGE('',*,*,#7217,.T.);
#10008=ORIENTED_EDGE('',*,*,#7219,.F.);
#10009=ORIENTED_EDGE('',*,*,#7209,.T.);
#10010=ORIENTED_EDGE('',*,*,#7220,.T.);
#10011=ORIENTED_EDGE('',*,*,#7218,.T.);
#10012=ORIENTED_EDGE('',*,*,#7220,.F.);
#10297=CYLINDRICAL_SURFACE('',#12653,0.35);
#10298=CYLINDRICAL_SURFACE('',#12661,0.1954);
#10890=ADVANCED_FACE('',(#1839),#1228,.F.);
#10891=ADVANCED_FACE('',(#1840),#1229,.F.);
#10892=ADVANCED_FACE('',(#1841),#1230,.F.);
#10893=ADVANCED_FACE('',(#1842),#1231,.F.);
#10894=ADVANCED_FACE('',(#1843),#1232,.F.);
#10895=ADVANCED_FACE('',(#1844),#1233,.F.);
#10896=ADVANCED_FACE('',(#1845),#1234,.F.);
#10897=ADVANCED_FACE('',(#1846),#1235,.F.);
#10898=ADVANCED_FACE('',(#1847),#1236,.F.);
#10899=ADVANCED_FACE('',(#1848),#1237,.T.);
#10900=ADVANCED_FACE('',(#1849),#509,.T.);
#10901=ADVANCED_FACE('',(#1850),#10297,.T.);
#10902=ADVANCED_FACE('',(#1851),#510,.T.);
#10903=ADVANCED_FACE('',(#1852,#887),#1238,.T.);
#10904=ADVANCED_FACE('',(#1853),#511,.T.);
#10905=ADVANCED_FACE('',(#1854),#10298,.T.);
#10979=CLOSED_SHELL('',(#10890,#10891,#10892,#10893,#10894,#10895,#10896,
#10897));
#10980=CLOSED_SHELL('',(#10898,#10899,#10900,#10901,#10902,#10903,#10904,
#10905));
#12638=AXIS2_PLACEMENT_3D('',#19756,#15891,#15892);
#12639=AXIS2_PLACEMENT_3D('',#19757,#15893,#15894);
#12640=AXIS2_PLACEMENT_3D('',#19766,#15899,#15900);
#12641=AXIS2_PLACEMENT_3D('',#19772,#15904,#15905);
#12642=AXIS2_PLACEMENT_3D('',#19778,#15909,#15910);
#12643=AXIS2_PLACEMENT_3D('',#19784,#15914,#15915);
#12644=AXIS2_PLACEMENT_3D('',#19790,#15919,#15920);
#12645=AXIS2_PLACEMENT_3D('',#19793,#15923,#15924);
#12646=AXIS2_PLACEMENT_3D('',#19794,#15925,#15926);
#12647=AXIS2_PLACEMENT_3D('',#19795,#15927,#15928);
#12648=AXIS2_PLACEMENT_3D('',#19797,#15929,#15930);
#12649=AXIS2_PLACEMENT_3D('',#19798,#15931,#15932);
#12650=AXIS2_PLACEMENT_3D('',#19800,#15933,#15934);
#12651=AXIS2_PLACEMENT_3D('',#19801,#15935,#15936);
#12652=AXIS2_PLACEMENT_3D('',#19803,#15937,#15938);
#12653=AXIS2_PLACEMENT_3D('',#19805,#15940,#15941);
#12654=AXIS2_PLACEMENT_3D('',#19807,#15942,#15943);
#12655=AXIS2_PLACEMENT_3D('',#19809,#15945,#15946);
#12656=AXIS2_PLACEMENT_3D('',#19811,#15947,#15948);
#12657=AXIS2_PLACEMENT_3D('',#19813,#15950,#15951);
#12658=AXIS2_PLACEMENT_3D('',#19815,#15952,#15953);
#12659=AXIS2_PLACEMENT_3D('',#19816,#15954,#15955);
#12660=AXIS2_PLACEMENT_3D('',#19818,#15956,#15957);
#12661=AXIS2_PLACEMENT_3D('',#19820,#15959,#15960);
#15891=DIRECTION('axis',(0.,0.,1.));
#15892=DIRECTION('refdir',(1.,0.,0.));
#15893=DIRECTION('center_axis',(0.866025403784439,0.,-0.5));
#15894=DIRECTION('ref_axis',(0.5,0.,0.866025403784439));
#15895=DIRECTION('',(-0.5,0.,-0.866025403784439));
#15896=DIRECTION('',(0.,-1.,0.));
#15897=DIRECTION('',(0.5,0.,0.866025403784439));
#15898=DIRECTION('',(0.,-1.,0.));
#15899=DIRECTION('center_axis',(1.60246890531964E-16,0.,-1.));
#15900=DIRECTION('ref_axis',(1.,0.,1.60246890531964E-16));
#15901=DIRECTION('',(-1.,0.,-1.60246890531964E-16));
#15902=DIRECTION('',(0.,-1.,0.));
#15903=DIRECTION('',(1.,0.,1.60246890531964E-16));
#15904=DIRECTION('center_axis',(-0.866025403784439,0.,-0.5));
#15905=DIRECTION('ref_axis',(0.5,0.,-0.866025403784439));
#15906=DIRECTION('',(-0.5,0.,0.866025403784439));
#15907=DIRECTION('',(0.,-1.,0.));
#15908=DIRECTION('',(0.5,0.,-0.866025403784439));
#15909=DIRECTION('center_axis',(-0.866025403784439,0.,0.5));
#15910=DIRECTION('ref_axis',(-0.5,0.,-0.866025403784439));
#15911=DIRECTION('',(0.5,0.,0.866025403784439));
#15912=DIRECTION('',(0.,-1.,0.));
#15913=DIRECTION('',(-0.5,0.,-0.866025403784439));
#15914=DIRECTION('center_axis',(-1.60246890531964E-16,0.,1.));
#15915=DIRECTION('ref_axis',(-1.,0.,-1.60246890531964E-16));
#15916=DIRECTION('',(1.,0.,1.60246890531964E-16));
#15917=DIRECTION('',(0.,-1.,0.));
#15918=DIRECTION('',(-1.,0.,-1.60246890531964E-16));
#15919=DIRECTION('center_axis',(0.866025403784439,0.,0.5));
#15920=DIRECTION('ref_axis',(-0.5,0.,0.866025403784439));
#15921=DIRECTION('',(0.5,0.,-0.866025403784439));
#15922=DIRECTION('',(-0.5,0.,0.866025403784439));
#15923=DIRECTION('center_axis',(0.,1.,0.));
#15924=DIRECTION('ref_axis',(1.,0.,0.));
#15925=DIRECTION('center_axis',(0.,-1.,0.));
#15926=DIRECTION('ref_axis',(0.,0.,-1.));
#15927=DIRECTION('center_axis',(0.,1.,0.));
#15928=DIRECTION('ref_axis',(1.,0.,0.));
#15929=DIRECTION('center_axis',(0.,1.,0.));
#15930=DIRECTION('ref_axis',(1.,0.,0.));
#15931=DIRECTION('center_axis',(0.,1.,0.));
#15932=DIRECTION('ref_axis',(0.,0.,1.));
#15933=DIRECTION('center_axis',(0.,-1.,0.));
#15934=DIRECTION('ref_axis',(1.,0.,0.));
#15935=DIRECTION('center_axis',(0.,-1.,0.));
#15936=DIRECTION('ref_axis',(1.,0.,0.));
#15937=DIRECTION('center_axis',(0.,-1.,0.));
#15938=DIRECTION('ref_axis',(1.,0.,0.));
#15939=DIRECTION('',(0.707106781186547,0.707106781186548,8.65956056235493E-17));
#15940=DIRECTION('center_axis',(0.,-1.,0.));
#15941=DIRECTION('ref_axis',(1.,0.,0.));
#15942=DIRECTION('center_axis',(0.,-1.,0.));
#15943=DIRECTION('ref_axis',(1.,0.,0.));
#15944=DIRECTION('',(0.,1.,0.));
#15945=DIRECTION('center_axis',(0.,1.,0.));
#15946=DIRECTION('ref_axis',(1.,0.,0.));
#15947=DIRECTION('center_axis',(0.,-1.,0.));
#15948=DIRECTION('ref_axis',(1.,0.,0.));
#15949=DIRECTION('',(-0.707106781186547,0.707106781186548,-8.65956056235493E-17));
#15950=DIRECTION('center_axis',(0.,-1.,0.));
#15951=DIRECTION('ref_axis',(0.,0.,-1.));
#15952=DIRECTION('center_axis',(0.,-1.,0.));
#15953=DIRECTION('ref_axis',(1.,0.,0.));
#15954=DIRECTION('center_axis',(0.,1.,0.));
#15955=DIRECTION('ref_axis',(1.,0.,0.));
#15956=DIRECTION('center_axis',(0.,1.,0.));
#15957=DIRECTION('ref_axis',(1.,0.,0.));
#15958=DIRECTION('',(-0.447213595499958,0.894427190999916,-5.47678698264203E-17));
#15959=DIRECTION('center_axis',(0.,-1.,0.));
#15960=DIRECTION('ref_axis',(1.,0.,0.));
#15961=DIRECTION('',(0.,1.,0.));
#19756=CARTESIAN_POINT('',(0.,0.,0.));
#19757=CARTESIAN_POINT('Origin',(0.0866025403784439,-0.4,-0.15));
#19758=CARTESIAN_POINT('',(0.173205080756888,-0.4,0.));
#19759=CARTESIAN_POINT('',(0.0866025403784439,-0.4,-0.15));
#19760=CARTESIAN_POINT('',(0.173205080756888,-0.4,0.));
#19761=CARTESIAN_POINT('',(0.0866025403784439,-0.64,-0.15));
#19762=CARTESIAN_POINT('',(0.0866025403784439,-0.4,-0.15));
#19763=CARTESIAN_POINT('',(0.173205080756888,-0.64,0.));
#19764=CARTESIAN_POINT('',(0.173205080756888,-0.64,0.));
#19765=CARTESIAN_POINT('',(0.173205080756888,-0.4,0.));
#19766=CARTESIAN_POINT('Origin',(-0.0866025403784438,-0.4,-0.15));
#19767=CARTESIAN_POINT('',(-0.0866025403784438,-0.4,-0.15));
#19768=CARTESIAN_POINT('',(0.0866025403784439,-0.4,-0.15));
#19769=CARTESIAN_POINT('',(-0.0866025403784438,-0.64,-0.15));
#19770=CARTESIAN_POINT('',(-0.0866025403784438,-0.4,-0.15));
#19771=CARTESIAN_POINT('',(0.0866025403784439,-0.64,-0.15));
#19772=CARTESIAN_POINT('Origin',(-0.173205080756888,-0.4,-2.77555756156289E-17));
#19773=CARTESIAN_POINT('',(-0.173205080756888,-0.4,-2.12115047744981E-17));
#19774=CARTESIAN_POINT('',(-0.0866025403784438,-0.4,-0.15));
#19775=CARTESIAN_POINT('',(-0.173205080756888,-0.64,-2.77555756156289E-17));
#19776=CARTESIAN_POINT('',(-0.173205080756888,-0.4,-2.12115047744981E-17));
#19777=CARTESIAN_POINT('',(-0.0866025403784438,-0.64,-0.15));
#19778=CARTESIAN_POINT('Origin',(-0.0866025403784439,-0.4,0.15));
#19779=CARTESIAN_POINT('',(-0.0866025403784439,-0.4,0.15));
#19780=CARTESIAN_POINT('',(-0.173205080756888,-0.4,-2.12115047744981E-17));
#19781=CARTESIAN_POINT('',(-0.0866025403784439,-0.64,0.15));
#19782=CARTESIAN_POINT('',(-0.0866025403784439,-0.4,0.15));
#19783=CARTESIAN_POINT('',(-0.173205080756888,-0.64,-2.12115047744981E-17));
#19784=CARTESIAN_POINT('Origin',(0.0866025403784439,-0.4,0.15));
#19785=CARTESIAN_POINT('',(0.0866025403784439,-0.4,0.15));
#19786=CARTESIAN_POINT('',(-0.0866025403784439,-0.4,0.15));
#19787=CARTESIAN_POINT('',(0.0866025403784439,-0.64,0.15));
#19788=CARTESIAN_POINT('',(0.0866025403784439,-0.4,0.15));
#19789=CARTESIAN_POINT('',(-0.0866025403784439,-0.64,0.15));
#19790=CARTESIAN_POINT('Origin',(0.173205080756888,-0.4,0.));
#19791=CARTESIAN_POINT('',(0.0866025403784439,-0.4,0.15));
#19792=CARTESIAN_POINT('',(0.0866025403784439,-0.64,0.15));
#19793=CARTESIAN_POINT('Origin',(0.,-0.4,-2.77555756156289E-17));
#19794=CARTESIAN_POINT('Origin',(0.,-0.64,-2.77555756156289E-17));
#19795=CARTESIAN_POINT('Origin',(0.,-1.,0.));
#19796=CARTESIAN_POINT('',(-0.1954,-1.,2.39295984553393E-17));
#19797=CARTESIAN_POINT('Origin',(0.,-1.,0.));
#19798=CARTESIAN_POINT('Origin',(0.3,0.4,0.));
#19799=CARTESIAN_POINT('',(-0.3,0.4,-3.67394039744206E-17));
#19800=CARTESIAN_POINT('Origin',(0.,0.4,0.));
#19801=CARTESIAN_POINT('Origin',(0.,0.375,0.));
#19802=CARTESIAN_POINT('',(-0.35,0.35,-4.28626379701573E-17));
#19803=CARTESIAN_POINT('Origin',(0.,0.35,0.));
#19804=CARTESIAN_POINT('',(-0.325,0.375,-3.9801020972289E-17));
#19805=CARTESIAN_POINT('Origin',(0.,0.19,0.));
#19806=CARTESIAN_POINT('',(-0.35,0.03,-4.28626379701574E-17));
#19807=CARTESIAN_POINT('Origin',(0.,0.03,0.));
#19808=CARTESIAN_POINT('',(-0.35,0.19,-4.28626379701574E-17));
#19809=CARTESIAN_POINT('Origin',(0.,0.0149999999999999,0.));
#19810=CARTESIAN_POINT('',(-0.32,-3.29597460435593E-17,-3.91886975727153E-17));
#19811=CARTESIAN_POINT('Origin',(0.,0.,0.));
#19812=CARTESIAN_POINT('',(-0.335,0.0149999999999999,-4.10256677714363E-17));
#19813=CARTESIAN_POINT('Origin',(0.22,0.,0.));
#19814=CARTESIAN_POINT('',(-0.22,-6.93889390390723E-18,-2.69422295812418E-17));
#19815=CARTESIAN_POINT('Origin',(0.,0.,0.));
#19816=CARTESIAN_POINT('Origin',(0.,-0.02,0.));
#19817=CARTESIAN_POINT('',(-0.1954,-0.0492,2.39295984553393E-17));
#19818=CARTESIAN_POINT('Origin',(0.,-0.0492,0.));
#19819=CARTESIAN_POINT('',(-0.21,-0.02,-2.57175827820944E-17));
#19820=CARTESIAN_POINT('Origin',(0.,-0.8,0.));
#19821=CARTESIAN_POINT('',(-0.1954,-0.8,-2.39295984553393E-17));
#20040=UNCERTAINTY_MEASURE_WITH_UNIT(LENGTH_MEASURE(0.001),#20097,
'DISTANCE_ACCURACY_VALUE',
'Maximum model space distance between geometric entities at asserted c
onnectivities');
#20042=UNCERTAINTY_MEASURE_WITH_UNIT(LENGTH_MEASURE(0.001),#20097,
'DISTANCE_ACCURACY_VALUE',
'Maximum model space distance between geometric entities at asserted c
onnectivities');
#20094=(
GEOMETRIC_REPRESENTATION_CONTEXT(3)
GLOBAL_UNCERTAINTY_ASSIGNED_CONTEXT((#20040))
GLOBAL_UNIT_ASSIGNED_CONTEXT((#20097,#20099,#20100))
REPRESENTATION_CONTEXT('','3D')
);
#20096=(
GEOMETRIC_REPRESENTATION_CONTEXT(3)
GLOBAL_UNCERTAINTY_ASSIGNED_CONTEXT((#20042))
GLOBAL_UNIT_ASSIGNED_CONTEXT((#20097,#20099,#20100))
REPRESENTATION_CONTEXT('','3D')
);
#20097=(
LENGTH_UNIT()
NAMED_UNIT(*)
SI_UNIT(.CENTI.,.METRE.)
);
#20099=(
NAMED_UNIT(*)
PLANE_ANGLE_UNIT()
SI_UNIT($,.RADIAN.)
);
#20100=(
NAMED_UNIT(*)
SI_UNIT($,.STERADIAN.)
SOLID_ANGLE_UNIT()
);
#20152=SHAPE_DEFINITION_REPRESENTATION(#20213,#20363);
#20213=PRODUCT_DEFINITION_SHAPE('',$,#20417);
#20363=SHAPE_REPRESENTATION('',(#12638),#20094);
#20365=PRODUCT_DEFINITION_CONTEXT('part definition',#20526,'design');
#20417=PRODUCT_DEFINITION('M4x10 Cap Screw','M4x10 Cap Screw',#20470,#20365);
#20470=PRODUCT_DEFINITION_FORMATION('',$,#20579);
#20526=APPLICATION_CONTEXT(
'Core Data for Automotive Mechanical Design Process');
#20527=PRODUCT_CONTEXT('part definition',#20526,'mechanical');
#20579=PRODUCT('M4x10 Cap Screw','M4x10 Cap Screw','M4x10 Cap Screw',(#20527));
#20651=COLOUR_RGB('Black',0.12,0.14,0.17);
#20652=FILL_AREA_STYLE_COLOUR('',#20651);
#20653=FILL_AREA_STYLE('',(#20652));
#20654=SURFACE_STYLE_FILL_AREA(#20653);
#20655=SURFACE_SIDE_STYLE('',(#20654));
#20656=SURFACE_STYLE_USAGE(.BOTH.,#20655);
#20657=PRESENTATION_STYLE_ASSIGNMENT((#20656));
ENDSEC;
END-ISO-10303-21;
